ISO-10303-21;
HEADER;
FILE_DESCRIPTION (('STEP AP214'),
    '1' );
FILE_NAME ('socket button head screw_iso_ISO 7380 - M5 x 20 - 20C.step',
    '2026-09-24T10:15:42',
    ( '' ),
    ( '' ),
    'SwSTEP 2.0',
    'SolidWorks 2026',
    '' );
FILE_SCHEMA (( 'AUTOMOTIVE_DESIGN' ));
ENDSEC;

DATA;
#102=VERTEX_POINT ( 'NONE', #10357 ) ;
#160=EDGE_CURVE ( 'NONE', #16571, #5854, #8950, .T. ) ;
#179=AXIS2_PLACEMENT_3D ( 'NONE', #11361, #10105, #14399 ) ;
#208=PLANE ( 'NONE',  #10210 ) ;
#214=AXIS2_PLACEMENT_3D ( 'NONE', #16612, #6578, #9348 ) ;
#217=( GEOMETRIC_REPRESENTATION_CONTEXT ( 3 ) GLOBAL_UNCERTAINTY_ASSIGNED_CONTEXT ( ( #16105 ) ) GLOBAL_UNIT_ASSIGNED_CONTEXT ( ( #3649, #3456, #9291 ) ) REPRESENTATION_CONTEXT ( 'NONE', 'WORKASPACE' ) );
#227=ORIENTED_EDGE ( 'NONE', *, *, #7719, .F. ) ;
#239=CYLINDRICAL_SURFACE ( 'NONE', #8737, 4.750000000000000000 ) ;
#300=DIRECTION ( 'NONE',  ( -0.000000000000000000, 1.000000000000000000, 1.224646799147353207E-16 ) ) ;
#320=DIRECTION ( 'NONE',  ( -0.000000000000000000, 0.000000000000000000, 1.000000000000000000 ) ) ;
#338=CARTESIAN_POINT ( 'NONE',  ( 1.560000000000000053, 0.8660254037844389297, -1.500000000000000000 ) ) ;
#344=AXIS2_PLACEMENT_3D ( 'NONE', #14911, #300, #1826 ) ;
#360=FACE_OUTER_BOUND ( 'NONE', #7164, .T. ) ;
#367=EDGE_LOOP ( 'NONE', ( #3917, #12671, #3001 ) ) ;
#388=EDGE_CURVE ( 'NONE', #11928, #8289, #18271, .T. ) ;
#409=AXIS2_PLACEMENT_3D ( 'NONE', #10692, #1287, #14297 ) ;
#417=ORIENTED_EDGE ( 'NONE', *, *, #14759, .F. ) ;
#493=DIRECTION ( 'NONE',  ( 0.000000000000000000, 0.000000000000000000, 1.000000000000000000 ) ) ;
#496=DIRECTION ( 'NONE',  ( 0.000000000000000000, 0.8660254037844384856, 0.5000000000000004441 ) ) ;
#544=AXIS2_PLACEMENT_3D ( 'NONE', #1365, #7303, #320 ) ;
#547=VECTOR ( 'NONE', #5418, 1000.000000000000000 ) ;
#551=ORIENTED_EDGE ( 'NONE', *, *, #11722, .F. ) ;
#579=ORIENTED_EDGE ( 'NONE', *, *, #14786, .T. ) ;
#641=ORIENTED_EDGE ( 'NONE', *, *, #13469, .F. ) ;
#672=LINE ( 'NONE', #13468, #4172 ) ;
#749=DIRECTION ( 'NONE',  ( 0.000000000000000000, 0.000000000000000000, -1.000000000000000000 ) ) ;
#768=VECTOR ( 'NONE', #1333, 1000.000000000000000 ) ;
#772=VECTOR ( 'NONE', #8614, 1000.000000000000114 ) ;
#773=EDGE_CURVE ( 'NONE', #1448, #13827, #16825, .T. ) ;
#784=( NAMED_UNIT ( * ) SI_UNIT ( $, .STERADIAN. ) SOLID_ANGLE_UNIT ( ) );
#809=( GEOMETRIC_REPRESENTATION_CONTEXT ( 3 ) GLOBAL_UNCERTAINTY_ASSIGNED_CONTEXT ( ( #4439 ) ) GLOBAL_UNIT_ASSIGNED_CONTEXT ( ( #6432, #13867, #784 ) ) REPRESENTATION_CONTEXT ( 'NONE', 'WORKASPACE' ) );
#829=AXIS2_PLACEMENT_3D ( 'NONE', #5389, #17325, #6923 ) ;
#841=ORIENTED_EDGE ( 'NONE', *, *, #5974, .T. ) ;
#863=PLANE ( 'NONE',  #7082 ) ;
#892=( GEOMETRIC_REPRESENTATION_CONTEXT ( 3 ) GLOBAL_UNCERTAINTY_ASSIGNED_CONTEXT ( ( #13048 ) ) GLOBAL_UNIT_ASSIGNED_CONTEXT ( ( #18467, #18375, #3851 ) ) REPRESENTATION_CONTEXT ( 'NONE', 'WORKASPACE' ) );
#903=DIRECTION ( 'NONE',  ( 0.000000000000000000, 0.000000000000000000, 1.000000000000000000 ) ) ;
#927=ORIENTED_EDGE ( 'NONE', *, *, #160, .T. ) ;
#960=CARTESIAN_POINT ( 'NONE',  ( 4.755015822784811164, -4.336808689942017736E-16, 0.000000000000000000 ) ) ;
#1020=EDGE_CURVE ( 'NONE', #2439, #16598, #1609, .T. ) ;
#1126=FACE_OUTER_BOUND ( 'NONE', #18409, .T. ) ;
#1157=TOROIDAL_SURFACE ( 'NONE', #15806, 2.700000000000000178, 0.2000000000000000111 ) ;
#1172=EDGE_LOOP ( 'NONE', ( #11818, #17072 ) ) ;
#1237=DIRECTION ( 'NONE',  ( 0.000000000000000000, 0.000000000000000000, -1.000000000000000000 ) ) ;
#1248=CARTESIAN_POINT ( 'NONE',  ( 1.560000000000000053, 1.732050807568878747, 7.017607234860990640E-28 ) ) ;
#1250=ORIENTED_EDGE ( 'NONE', *, *, #18133, .T. ) ;
#1287=DIRECTION ( 'NONE',  ( -1.000000000000000000, -0.000000000000000000, -0.000000000000000000 ) ) ;
#1333=DIRECTION ( 'NONE',  ( -1.000000000000000000, -0.000000000000000000, -0.000000000000000000 ) ) ;
#1358=VECTOR ( 'NONE', #13265, 1000.000000000000000 ) ;
#1365=CARTESIAN_POINT ( 'NONE',  ( 2.750000000000000000, 2.499999999999999112, 0.000000000000000000 ) ) ;
#1439=CIRCLE ( 'NONE', #6339, 2.500000000000000000 ) ;
#1448=VERTEX_POINT ( 'NONE', #12732 ) ;
#1480=LINE ( 'NONE', #5326, #547 ) ;
#1495=ORIENTED_EDGE ( 'NONE', *, *, #11782, .T. ) ;
#1515=EDGE_CURVE ( 'NONE', #7837, #3148, #11224, .T. ) ;
#1523=CARTESIAN_POINT ( 'NONE',  ( 0.000000000000000000, 0.000000000000000000, 4.750000000000000000 ) ) ;
#1538=LINE ( 'NONE', #7377, #13330 ) ;
#1556=PLANE ( 'NONE',  #544 ) ;
#1567=ADVANCED_FACE ( 'NONE', ( #15784 ), #7481, .T. ) ;
#1582=EDGE_LOOP ( 'NONE', ( #7819, #4815, #18205 ) ) ;
#1597=CIRCLE ( 'NONE', #7097, 1.500000000000000000 ) ;
#1609=LINE ( 'NONE', #7746, #1358 ) ;
#1636=CARTESIAN_POINT ( 'NONE',  ( 1.560000000000000053, -1.732050807568877859, -1.752539433813135784E-17 ) ) ;
#1730=AXIS2_PLACEMENT_3D ( 'NONE', #2023, #7862, #7960 ) ;
#1744=CIRCLE ( 'NONE', #12429, 2.375000000000000444 ) ;
#1745=AXIS2_PLACEMENT_3D ( 'NONE', #8090, #7914, #16505 ) ;
#1758=VECTOR ( 'NONE', #10835, 1000.000000000000114 ) ;
#1817=CARTESIAN_POINT ( 'NONE',  ( 1.560000000000000053, 1.732050807568878747, 7.017607234860990640E-28 ) ) ;
#1824=VECTOR ( 'NONE', #11466, 1000.000000000000000 ) ;
#1826=DIRECTION ( 'NONE',  ( 0.000000000000000000, -1.224646799147353207E-16, 1.000000000000000000 ) ) ;
#1845=SURFACE_STYLE_USAGE ( .BOTH. , #6526 ) ;
#1859=DIRECTION ( 'NONE',  ( 0.000000000000000000, 0.000000000000000000, 1.000000000000000000 ) ) ;
#1952=ORIENTED_EDGE ( 'NONE', *, *, #15219, .F. ) ;
#1953=ORIENTED_EDGE ( 'NONE', *, *, #15909, .T. ) ;
#1958=ORIENTED_EDGE ( 'NONE', *, *, #15429, .F. ) ;
#1986=PRODUCT_DEFINITION_CONTEXT ( 'detailed design', #3750, 'design' ) ;
#2006=VECTOR ( 'NONE', #13244, 1000.000000000000000 ) ;
#2008=DIRECTION ( 'NONE',  ( -1.000000000000000000, 0.000000000000000000, 0.000000000000000000 ) ) ;
#2023=CARTESIAN_POINT ( 'NONE',  ( -997.5739745962155212, 0.000000000000000000, 0.000000000000000000 ) ) ;
#2030=AXIS2_PLACEMENT_3D ( 'NONE', #15716, #11248, #17249 ) ;
#2040=ORIENTED_EDGE ( 'NONE', *, *, #15270, .T. ) ;
#2133=FILL_AREA_STYLE_COLOUR ( '', #11487 ) ;
#2171=ORIENTED_EDGE ( 'NONE', *, *, #3888, .T. ) ;
#2226=EDGE_CURVE ( 'NONE', #13902, #8289, #14775, .T. ) ;
#2241=DIRECTION ( 'NONE',  ( 0.000000000000000000, 0.000000000000000000, 1.000000000000000000 ) ) ;
#2266=ORIENTED_EDGE ( 'NONE', *, *, #2226, .T. ) ;
#2332=EDGE_CURVE ( 'NONE', #15040, #13838, #14791, .T. ) ;
#2334=CARTESIAN_POINT ( 'NONE',  ( 22.30499999999999972, 0.000000000000000000, 0.000000000000000000 ) ) ;
#2347=CIRCLE ( 'NONE', #17294, 4.750000000000000000 ) ;
#2381=LINE ( 'NONE', #18432, #8014 ) ;
#2402=ORIENTED_EDGE ( 'NONE', *, *, #14786, .F. ) ;
#2409=SURFACE_STYLE_FILL_AREA ( #3573 ) ;
#2437=ORIENTED_EDGE ( 'NONE', *, *, #12827, .F. ) ;
#2439=VERTEX_POINT ( 'NONE', #18580 ) ;
#2447=FACE_OUTER_BOUND ( 'NONE', #4107, .T. ) ;
#2449=ORIENTED_EDGE ( 'NONE', *, *, #15428, .T. ) ;
#2475=CYLINDRICAL_SURFACE ( 'NONE', #6597, 4.750000000000000000 ) ;
#2490=CARTESIAN_POINT ( 'NONE',  ( 0.000000000000000000, 1.732050807568878747, 7.017607234860990640E-28 ) ) ;
#2493=CIRCLE ( 'NONE', #11370, 2.055000000000000160 ) ;
#2508=ORIENTED_EDGE ( 'NONE', *, *, #4966, .F. ) ;
#2584=ORIENTED_EDGE ( 'NONE', *, *, #17542, .F. ) ;
#2591=ORIENTED_EDGE ( 'NONE', *, *, #12297, .F. ) ;
#2625=ORIENTED_EDGE ( 'NONE', *, *, #7208, .F. ) ;
#2646=ORIENTED_EDGE ( 'NONE', *, *, #11722, .T. ) ;
#2667=DIRECTION ( 'NONE',  ( -0.5000000000000042188, 1.060575238724903710E-16, -0.8660254037844361541 ) ) ;
#2714=VECTOR ( 'NONE', #18374, 1000.000000000000000 ) ;
#2718=ORIENTED_EDGE ( 'NONE', *, *, #7759, .T. ) ;
#2719=ORIENTED_EDGE ( 'NONE', *, *, #4263, .T. ) ;
#2729=DIRECTION ( 'NONE',  ( -0.000000000000000000, -1.000000000000000000, -0.000000000000000000 ) ) ;
#2759=CIRCLE ( 'NONE', #344, 0.2000000000000000944 ) ;
#2761=FACE_BOUND ( 'NONE', #10743, .T. ) ;
#2777=CARTESIAN_POINT ( 'NONE',  ( 1.560000000000000053, 0.8660254037844389297, 1.500000000000000000 ) ) ;
#2838=DIRECTION ( 'NONE',  ( 0.000000000000000000, 1.000000000000000000, 1.224646799147353454E-16 ) ) ;
#2851=ORIENTED_EDGE ( 'NONE', *, *, #7066, .T. ) ;
#2877=CIRCLE ( 'NONE', #12359, 1.500000000000000000 ) ;
#2891=CARTESIAN_POINT ( 'NONE',  ( 22.75000000000000000, 2.789133085058097101E-16, -2.055000000000000160 ) ) ;
#2969=EDGE_CURVE ( 'NONE', #6750, #3366, #672, .T. ) ;
#2972=LINE ( 'NONE', #8819, #9982 ) ;
#3001=ORIENTED_EDGE ( 'NONE', *, *, #6952, .F. ) ;
#3023=FACE_OUTER_BOUND ( 'NONE', #6790, .T. ) ;
#3104=DIRECTION ( 'NONE',  ( 0.000000000000000000, 0.000000000000000000, 1.000000000000000000 ) ) ;
#3121=DIRECTION ( 'NONE',  ( 0.000000000000000000, 0.000000000000000000, -1.000000000000000000 ) ) ;
#3148=VERTEX_POINT ( 'NONE', #6501 ) ;
#3221=EDGE_CURVE ( 'NONE', #16117, #12360, #17266, .T. ) ;
#3279=FACE_OUTER_BOUND ( 'NONE', #13417, .T. ) ;
#3305=CARTESIAN_POINT ( 'NONE',  ( 22.75000000000000000, 0.000000000000000000, 2.055000000000000160 ) ) ;
#3308=CARTESIAN_POINT ( 'NONE',  ( 1.560000000000000053, 0.000000000000000000, 2.999999999999998668 ) ) ;
#3366=VERTEX_POINT ( 'NONE', #8296 ) ;
#3440=ORIENTED_EDGE ( 'NONE', *, *, #5774, .F. ) ;
#3456=( NAMED_UNIT ( * ) PLANE_ANGLE_UNIT ( ) SI_UNIT ( $, .RADIAN. ) );
#3467=ORIENTED_EDGE ( 'NONE', *, *, #2969, .T. ) ;
#3472=ORIENTED_EDGE ( 'NONE', *, *, #12827, .T. ) ;
#3522=EDGE_CURVE ( 'NONE', #6750, #1448, #11799, .T. ) ;
#3531=DIRECTION ( 'NONE',  ( -1.000000000000000000, 0.000000000000000000, 0.000000000000000000 ) ) ;
#3541=DIRECTION ( 'NONE',  ( 0.000000000000000000, -0.5000000000000003331, 0.8660254037844383745 ) ) ;
#3573=FILL_AREA_STYLE ('',( #10851 ) ) ;
#3596=VERTEX_POINT ( 'NONE', #6257 ) ;
#3618=CARTESIAN_POINT ( 'NONE',  ( 1.560000000000000053, -1.732050807568877859, -1.752539433813135784E-17 ) ) ;
#3621=DIRECTION ( 'NONE',  ( 0.000000000000000000, 0.000000000000000000, 1.000000000000000000 ) ) ;
#3629=DIRECTION ( 'NONE',  ( 0.000000000000000000, 0.000000000000000000, 1.000000000000000000 ) ) ;
#3636=COLOUR_RGB ( '', 0.09019608, 0.27058824, 0.51372549) ;
#3647=EDGE_CURVE ( 'NONE', #10742, #3366, #4032, .T. ) ;
#3649=( LENGTH_UNIT ( ) NAMED_UNIT ( * ) SI_UNIT ( .MILLI., .METRE. ) );
#3698=ORIENTED_EDGE ( 'NONE', *, *, #8087, .T. ) ;
#3750=APPLICATION_CONTEXT ( 'automotive_design' ) ;
#3762=AXIS2_PLACEMENT_3D ( 'NONE', #17444, #10467, #18870 ) ;
#3784=VECTOR ( 'NONE', #13274, 1000.000000000000000 ) ;
#3851=( NAMED_UNIT ( * ) SI_UNIT ( $, .STERADIAN. ) SOLID_ANGLE_UNIT ( ) );
#3857=STYLED_ITEM ( 'NONE', ( #12344 ), #14891 ) ;
#3888=EDGE_CURVE ( 'NONE', #8289, #18437, #16467, .T. ) ;
#3917=ORIENTED_EDGE ( 'NONE', *, *, #14530, .F. ) ;
#3951=ADVANCED_FACE ( 'NONE', ( #4012 ), #11104, .T. ) ;
#4012=FACE_OUTER_BOUND ( 'NONE', #17823, .T. ) ;
#4014=FACE_OUTER_BOUND ( 'NONE', #15355, .T. ) ;
#4025=EDGE_CURVE ( 'NONE', #15040, #10542, #4875, .T. ) ;
#4031=DIRECTION ( 'NONE',  ( -0.000000000000000000, 0.5000000000000003331, -0.8660254037844384856 ) ) ;
#4032=LINE ( 'NONE', #2490, #2714 ) ;
#4073=EDGE_LOOP ( 'NONE', ( #15628, #15422, #18222, #4846 ) ) ;
#4107=EDGE_LOOP ( 'NONE', ( #5226, #8780, #10476 ) ) ;
#4172=VECTOR ( 'NONE', #3531, 1000.000000000000000 ) ;
#4263=EDGE_CURVE ( 'NONE', #10243, #9140, #9077, .T. ) ;
#4266=CARTESIAN_POINT ( 'NONE',  ( 2.369999999999999662, 0.000000000000000000, 0.000000000000000000 ) ) ;
#4273=LINE ( 'NONE', #5879, #2006 ) ;
#4293=ORIENTED_EDGE ( 'NONE', *, *, #388, .T. ) ;
#4327=DIRECTION ( 'NONE',  ( 0.000000000000000000, 0.000000000000000000, 1.000000000000000000 ) ) ;
#4394=DIRECTION ( 'NONE',  ( -1.000000000000000000, -0.000000000000000000, -0.000000000000000000 ) ) ;
#4439=UNCERTAINTY_MEASURE_WITH_UNIT (LENGTH_MEASURE( 1.000000000000000082E-05 ), #6432, 'distance_accuracy_value', 'NONE');
#4442=FACE_OUTER_BOUND ( 'NONE', #11414, .T. ) ;
#4465=CARTESIAN_POINT ( 'NONE',  ( 4.755015822784811164, -4.336808689942017736E-16, 0.000000000000000000 ) ) ;
#4507=VERTEX_POINT ( 'NONE', #12866 ) ;
#4659=DIRECTION ( 'NONE',  ( 1.000000000000000000, 0.000000000000000000, 0.000000000000000000 ) ) ;
#4669=CONICAL_SURFACE ( 'NONE', #7457, 2.055000000000000160, 0.7853981633974482790 ) ;
#4690=EDGE_CURVE ( 'NONE', #6415, #10542, #7147, .T. ) ;
#4761=CARTESIAN_POINT ( 'NONE',  ( 2.369999999999999662, 4.749999999999999112, 0.000000000000000000 ) ) ;
#4768=CARTESIAN_POINT ( 'NONE',  ( 1.560000000000000053, 0.000000000000000000, 0.000000000000000000 ) ) ;
#4774=ORIENTED_EDGE ( 'NONE', *, *, #3647, .T. ) ;
#4815=ORIENTED_EDGE ( 'NONE', *, *, #1020, .F. ) ;
#4846=ORIENTED_EDGE ( 'NONE', *, *, #3888, .F. ) ;
#4875=CIRCLE ( 'NONE', #16472, 5.315148208181396328 ) ;
#4890=EDGE_LOOP ( 'NONE', ( #1495, #927 ) ) ;
#4933=AXIS2_PLACEMENT_3D ( 'NONE', #13677, #13568, #493 ) ;
#4962=AXIS2_PLACEMENT_3D ( 'NONE', #11330, #11518, #749 ) ;
#4966=EDGE_CURVE ( 'NONE', #18645, #2439, #11749, .T. ) ;
#4976=DIRECTION ( 'NONE',  ( -0.000000000000000000, 0.5000000000000003331, -0.8660254037844384856 ) ) ;
#4988=AXIS2_PLACEMENT_3D ( 'NONE', #5741, #12922, #4327 ) ;
#5065=ORIENTED_EDGE ( 'NONE', *, *, #4690, .F. ) ;
#5066=CARTESIAN_POINT ( 'NONE',  ( 1.560000000000000053, -0.8660254037844384856, -1.500000000000000000 ) ) ;
#5069=AXIS2_PLACEMENT_3D ( 'NONE', #9801, #13931, #3621 ) ;
#5085=DIRECTION ( 'NONE',  ( 0.000000000000000000, 0.000000000000000000, 1.000000000000000000 ) ) ;
#5093=CIRCLE ( 'NONE', #15766, 4.750000000000000000 ) ;
#5173=CIRCLE ( 'NONE', #9454, 5.315148208181397216 ) ;
#5226=ORIENTED_EDGE ( 'NONE', *, *, #4263, .F. ) ;
#5230=LINE ( 'NONE', #18862, #15334 ) ;
#5243=CARTESIAN_POINT ( 'NONE',  ( 2.949999999999999734, 0.000000000000000000, 2.500000000000000000 ) ) ;
#5252=CARTESIAN_POINT ( 'NONE',  ( 1.560000000000000053, 0.000000000000000000, 2.999999999999998668 ) ) ;
#5278=ORIENTED_EDGE ( 'NONE', *, *, #7573, .F. ) ;
#5293=CARTESIAN_POINT ( 'NONE',  ( 0.000000000000000000, 0.8660254037844389297, -1.500000000000000000 ) ) ;
#5298=AXIS2_PLACEMENT_3D ( 'NONE', #2334, #7105, #903 ) ;
#5326=CARTESIAN_POINT ( 'NONE',  ( 1.560000000000000053, -0.8660254037844384856, 1.500000000000000000 ) ) ;
#5329=AXIS2_PLACEMENT_3D ( 'NONE', #10143, #7290, #8994 ) ;
#5370=ADVANCED_FACE ( 'NONE', ( #12619, #2761 ), #14433, .T. ) ;
#5389=CARTESIAN_POINT ( 'NONE',  ( 1.560000000000000053, 0.000000000000000000, 0.000000000000000000 ) ) ;
#5402=CIRCLE ( 'NONE', #16088, 1.500000000000000000 ) ;
#5418=DIRECTION ( 'NONE',  ( -1.000000000000000000, 0.000000000000000000, 0.000000000000000000 ) ) ;
#5458=DIRECTION ( 'NONE',  ( -1.000000000000000000, -0.000000000000000000, -0.000000000000000000 ) ) ;
#5509=FACE_OUTER_BOUND ( 'NONE', #7867, .T. ) ;
#5519=VECTOR ( 'NONE', #5794, 1000.000000000000000 ) ;
#5525=DIRECTION ( 'NONE',  ( 0.000000000000000000, 0.000000000000000000, 1.000000000000000000 ) ) ;
#5540=EDGE_CURVE ( 'NONE', #6435, #7502, #1538, .T. ) ;
#5552=EDGE_LOOP ( 'NONE', ( #13053, #17280, #10056, #14941, #7334 ) ) ;
#5608=DIRECTION ( 'NONE',  ( 0.000000000000000000, 1.000000000000000000, 0.000000000000000000 ) ) ;
#5619=DIRECTION ( 'NONE',  ( -1.000000000000000000, -0.000000000000000000, -0.000000000000000000 ) ) ;
#5622=DIRECTION ( 'NONE',  ( -1.000000000000000000, -0.000000000000000000, -0.000000000000000000 ) ) ;
#5624=CONICAL_SURFACE ( 'NONE', #7497, 1732.050807568857181, 1.047197551196592746 ) ;
#5733=DIRECTION ( 'NONE',  ( -1.000000000000000000, 0.000000000000000000, 0.000000000000000000 ) ) ;
#5741=CARTESIAN_POINT ( 'NONE',  ( 1.560000000000000053, 0.000000000000000000, 2.999999999999998668 ) ) ;
#5756=DIRECTION ( 'NONE',  ( -0.000000000000000000, -0.5000000000000003331, -0.8660254037844384856 ) ) ;
#5774=EDGE_CURVE ( 'NONE', #13838, #13455, #5093, .T. ) ;
#5778=EDGE_LOOP ( 'NONE', ( #2508, #2646, #841, #2040, #1250 ) ) ;
#5794=DIRECTION ( 'NONE',  ( -0.000000000000000000, 1.000000000000000000, -0.000000000000000000 ) ) ;
#5829=PRODUCT_DEFINITION_SHAPE ( 'NONE', 'NONE',  #9645 ) ;
#5832=DIRECTION ( 'NONE',  ( 0.000000000000000000, 0.5000000000000003331, 0.8660254037844383745 ) ) ;
#5835=ADVANCED_FACE ( 'NONE', ( #15054 ), #10287, .T. ) ;
#5840=PLANE ( 'NONE',  #17495 ) ;
#5854=VERTEX_POINT ( 'NONE', #6273 ) ;
#5879=CARTESIAN_POINT ( 'NONE',  ( 1.560000000000000053, 0.8660254037844389297, -1.500000000000000000 ) ) ;
#5915=DIRECTION ( 'NONE',  ( 0.000000000000000000, 0.000000000000000000, 1.000000000000000000 ) ) ;
#5974=EDGE_CURVE ( 'NONE', #18680, #3148, #5402, .T. ) ;
#6011=VECTOR ( 'NONE', #4976, 1000.000000000000114 ) ;
#6068=CARTESIAN_POINT ( 'NONE',  ( 0.000000000000000000, 0.000000000000000000, 0.000000000000000000 ) ) ;
#6132=LINE ( 'NONE', #5066, #6011 ) ;
#6151=ORIENTED_EDGE ( 'NONE', *, *, #7719, .T. ) ;
#6257=CARTESIAN_POINT ( 'NONE',  ( 1.560000000000000053, -1.299038105676658450, 0.7500000000000007772 ) ) ;
#6270=VECTOR ( 'NONE', #7822, 1000.000000000000000 ) ;
#6273=CARTESIAN_POINT ( 'NONE',  ( 2.750000000000000000, 0.000000000000000000, 2.700000000000000178 ) ) ;
#6289=DIRECTION ( 'NONE',  ( 0.000000000000000000, 0.000000000000000000, 1.000000000000000000 ) ) ;
#6304=CARTESIAN_POINT ( 'NONE',  ( 1.560000000000000053, 0.8660254037844389297, -1.500000000000000000 ) ) ;
#6339=AXIS2_PLACEMENT_3D ( 'NONE', #17346, #14200, #15536 ) ;
#6340=EDGE_CURVE ( 'NONE', #7837, #4507, #8067, .T. ) ;
#6371=EDGE_CURVE ( 'NONE', #9140, #6750, #7891, .T. ) ;
#6392=ORIENTED_EDGE ( 'NONE', *, *, #1020, .T. ) ;
#6415=VERTEX_POINT ( 'NONE', #17117 ) ;
#6419=PLANE ( 'NONE',  #16701 ) ;
#6432=( LENGTH_UNIT ( ) NAMED_UNIT ( * ) SI_UNIT ( .MILLI., .METRE. ) );
#6435=VERTEX_POINT ( 'NONE', #8338 ) ;
#6437=SHAPE_REPRESENTATION ( 'socket button head screw_iso_ISO 7380 - M5 x 20 - 20C', ( #2030 ), #809 ) ;
#6466=ADVANCED_FACE ( 'NONE', ( #8519 ), #18553, .T. ) ;
#6480=AXIS2_PLACEMENT_3D ( 'NONE', #1248, #12813, #15964 ) ;
#6501=CARTESIAN_POINT ( 'NONE',  ( 1.560000000000000053, -1.299038105676658450, -0.7500000000000007772 ) ) ;
#6526=SURFACE_SIDE_STYLE ('',( #12169 ) ) ;
#6578=DIRECTION ( 'NONE',  ( 1.000000000000000000, 0.000000000000000000, 0.000000000000000000 ) ) ;
#6597=AXIS2_PLACEMENT_3D ( 'NONE', #8691, #11660, #17485 ) ;
#6603=ORIENTED_EDGE ( 'NONE', *, *, #5540, .F. ) ;
#6614=DIRECTION ( 'NONE',  ( 0.000000000000000000, 0.000000000000000000, 1.000000000000000000 ) ) ;
#6701=ADVANCED_FACE ( 'NONE', ( #8137 ), #863, .T. ) ;
#6707=EDGE_CURVE ( 'NONE', #13827, #16117, #2381, .T. ) ;
#6747=ADVANCED_FACE ( 'NONE', ( #3023 ), #18431, .T. ) ;
#6750=VERTEX_POINT ( 'NONE', #17377 ) ;
#6790=EDGE_LOOP ( 'NONE', ( #15670, #17779, #17222, #16385, #13948 ) ) ;
#6819=CIRCLE ( 'NONE', #5298, 2.500000000000000888 ) ;
#6861=VECTOR ( 'NONE', #7362, 1000.000000000000000 ) ;
#6923=DIRECTION ( 'NONE',  ( 0.000000000000000000, 0.000000000000000000, 1.000000000000000000 ) ) ;
#6952=EDGE_CURVE ( 'NONE', #2439, #1448, #1597, .T. ) ;
#6972=CARTESIAN_POINT ( 'NONE',  ( 1.560000000000000053, 0.8660254037844389297, -1.500000000000000000 ) ) ;
#7014=VECTOR ( 'NONE', #13132, 1000.000000000000000 ) ;
#7066=EDGE_CURVE ( 'NONE', #16598, #3596, #5230, .T. ) ;
#7082=AXIS2_PLACEMENT_3D ( 'NONE', #5252, #11095, #16913 ) ;
#7097=AXIS2_PLACEMENT_3D ( 'NONE', #4768, #14987, #10794 ) ;
#7100=EDGE_CURVE ( 'NONE', #5854, #18437, #9537, .T. ) ;
#7105=DIRECTION ( 'NONE',  ( -1.000000000000000000, -0.000000000000000000, -0.000000000000000000 ) ) ;
#7147=CIRCLE ( 'NONE', #9868, 2.375000000000000444 ) ;
#7153=DIRECTION ( 'NONE',  ( 1.000000000000000000, 0.000000000000000000, -0.000000000000000000 ) ) ;
#7160=CARTESIAN_POINT ( 'NONE',  ( 0.000000000000000000, 0.8660254037844389297, 1.500000000000000000 ) ) ;
#7164=EDGE_LOOP ( 'NONE', ( #14395, #8002, #10059 ) ) ;
#7175=AXIS2_PLACEMENT_3D ( 'NONE', #11825, #10586, #3104 ) ;
#7208=EDGE_CURVE ( 'NONE', #10123, #13902, #2493, .T. ) ;
#7228=CARTESIAN_POINT ( 'NONE',  ( 22.75000000000000000, 0.000000000000000000, 2.055000000000000160 ) ) ;
#7290=DIRECTION ( 'NONE',  ( 0.000000000000000000, 0.000000000000000000, -1.000000000000000000 ) ) ;
#7299=PLANE ( 'NONE',  #4988 ) ;
#7303=DIRECTION ( 'NONE',  ( -1.000000000000000000, 0.000000000000000000, -0.000000000000000000 ) ) ;
#7334=ORIENTED_EDGE ( 'NONE', *, *, #2969, .F. ) ;
#7337=ORIENTED_EDGE ( 'NONE', *, *, #18211, .F. ) ;
#7362=DIRECTION ( 'NONE',  ( -1.000000000000000000, -0.000000000000000000, -0.000000000000000000 ) ) ;
#7377=CARTESIAN_POINT ( 'NONE',  ( 1.560000000000000053, -0.8660254037844384856, -1.500000000000000000 ) ) ;
#7392=VECTOR ( 'NONE', #13786, 1000.000000000000000 ) ;
#7394=DIRECTION ( 'NONE',  ( 0.000000000000000000, -0.8660254037844384856, -0.5000000000000004441 ) ) ;
#7420=EDGE_CURVE ( 'NONE', #3596, #7837, #10044, .T. ) ;
#7453=ADVANCED_FACE ( 'NONE', ( #8523 ), #14348, .T. ) ;
#7457=AXIS2_PLACEMENT_3D ( 'NONE', #12594, #15839, #18520 ) ;
#7468=ORIENTED_EDGE ( 'NONE', *, *, #17300, .F. ) ;
#7474=ADVANCED_FACE ( 'NONE', ( #17801 ), #208, .T. ) ;
#7481=PLANE ( 'NONE',  #16083 ) ;
#7482=VECTOR ( 'NONE', #17557, 1000.000000000000114 ) ;
#7497=AXIS2_PLACEMENT_3D ( 'NONE', #12478, #16521, #6289 ) ;
#7502=VERTEX_POINT ( 'NONE', #15754 ) ;
#7573=EDGE_CURVE ( 'NONE', #1448, #9140, #14796, .T. ) ;
#7719=EDGE_CURVE ( 'NONE', #14456, #13838, #14605, .T. ) ;
#7746=CARTESIAN_POINT ( 'NONE',  ( 1.560000000000000053, -0.8660254037844384856, 1.500000000000000000 ) ) ;
#7759=EDGE_CURVE ( 'NONE', #10243, #10742, #15089, .T. ) ;
#7785=EDGE_LOOP ( 'NONE', ( #11308, #2625 ) ) ;
#7814=DIRECTION ( 'NONE',  ( -1.000000000000000000, -0.000000000000000000, -0.000000000000000000 ) ) ;
#7819=ORIENTED_EDGE ( 'NONE', *, *, #7066, .F. ) ;
#7822=DIRECTION ( 'NONE',  ( -0.000000000000000000, -0.5000000000000004441, 0.8660254037844383745 ) ) ;
#7835=ORIENTED_EDGE ( 'NONE', *, *, #14863, .F. ) ;
#7837=VERTEX_POINT ( 'NONE', #3618 ) ;
#7844=DIRECTION ( 'NONE',  ( -0.5000000000000042188, 0.000000000000000000, 0.8660254037844361541 ) ) ;
#7862=DIRECTION ( 'NONE',  ( -1.000000000000000000, -0.000000000000000000, -0.000000000000000000 ) ) ;
#7867=EDGE_LOOP ( 'NONE', ( #11990, #15210, #9971, #10064 ) ) ;
#7891=LINE ( 'NONE', #13701, #7392 ) ;
#7914=DIRECTION ( 'NONE',  ( -1.000000000000000000, -0.000000000000000000, -0.000000000000000000 ) ) ;
#7945=AXIS2_PLACEMENT_3D ( 'NONE', #9747, #15300, #6614 ) ;
#7960=DIRECTION ( 'NONE',  ( 0.000000000000000000, 0.000000000000000000, 1.000000000000000000 ) ) ;
#7982=ORIENTED_EDGE ( 'NONE', *, *, #11782, .F. ) ;
#8002=ORIENTED_EDGE ( 'NONE', *, *, #7420, .F. ) ;
#8014=VECTOR ( 'NONE', #11191, 1000.000000000000000 ) ;
#8017=EDGE_CURVE ( 'NONE', #18680, #10243, #4273, .T. ) ;
#8067=LINE ( 'NONE', #13875, #9526 ) ;
#8087=EDGE_CURVE ( 'NONE', #3366, #16117, #13437, .T. ) ;
#8090=CARTESIAN_POINT ( 'NONE',  ( 2.949999999999999734, 0.000000000000000000, 0.000000000000000000 ) ) ;
#8137=FACE_OUTER_BOUND ( 'NONE', #18502, .T. ) ;
#8257=ORIENTED_EDGE ( 'NONE', *, *, #2332, .F. ) ;
#8266=PRODUCT_CONTEXT ( 'NONE', #16819, 'mechanical' ) ;
#8271=CARTESIAN_POINT ( 'NONE',  ( 1.560000000000000053, 0.000000000000000000, 0.000000000000000000 ) ) ;
#8289=VERTEX_POINT ( 'NONE', #9258 ) ;
#8296=CARTESIAN_POINT ( 'NONE',  ( 0.000000000000000000, 1.732050807568878747, 7.017607234860990640E-28 ) ) ;
#8308=CARTESIAN_POINT ( 'NONE',  ( 2.750000000000000000, 0.000000000000000000, 4.750000000000000000 ) ) ;
#8322=DIRECTION ( 'NONE',  ( -1.000000000000000000, -0.000000000000000000, -0.000000000000000000 ) ) ;
#8338=CARTESIAN_POINT ( 'NONE',  ( 1.560000000000000053, -0.8660254037844384856, -1.500000000000000000 ) ) ;
#8340=ORIENTED_EDGE ( 'NONE', *, *, #14863, .T. ) ;
#8426=CARTESIAN_POINT ( 'NONE',  ( 1.560000000000000053, -1.732050807568877859, -1.752539433813135784E-17 ) ) ;
#8427=ORIENTED_EDGE ( 'NONE', *, *, #15219, .T. ) ;
#8513=CARTESIAN_POINT ( 'NONE',  ( 2.426025403784448642, 2.655529440325959183E-32, -2.168404344971008868E-16 ) ) ;
#8519=FACE_OUTER_BOUND ( 'NONE', #17814, .T. ) ;
#8523=FACE_OUTER_BOUND ( 'NONE', #14812, .T. ) ;
#8542=ADVANCED_FACE ( 'NONE', ( #2447 ), #11265, .T. ) ;
#8560=ORIENTED_EDGE ( 'NONE', *, *, #7208, .T. ) ;
#8588=CARTESIAN_POINT ( 'NONE',  ( 1.560000000000000053, 0.8660254037844389297, 1.500000000000000000 ) ) ;
#8614=DIRECTION ( 'NONE',  ( -0.000000000000000000, -0.5000000000000003331, -0.8660254037844384856 ) ) ;
#8691=CARTESIAN_POINT ( 'NONE',  ( 0.000000000000000000, 0.000000000000000000, 0.000000000000000000 ) ) ;
#8737=AXIS2_PLACEMENT_3D ( 'NONE', #6068, #11897, #17733 ) ;
#8780=ORIENTED_EDGE ( 'NONE', *, *, #8017, .F. ) ;
#8819=CARTESIAN_POINT ( 'NONE',  ( 22.75000000000000000, 2.516649172247811061E-16, -2.055000000000000160 ) ) ;
#8842=CARTESIAN_POINT ( 'NONE',  ( 2.369999999999999662, 0.000000000000000000, 4.750000000000000000 ) ) ;
#8877=EDGE_LOOP ( 'NONE', ( #12837, #1953, #15406, #1958, #10718 ) ) ;
#8902=AXIS2_PLACEMENT_3D ( 'NONE', #11649, #3121, #5608 ) ;
#8949=CARTESIAN_POINT ( 'NONE',  ( 0.000000000000000000, 0.000000000000000000, 0.000000000000000000 ) ) ;
#8950=CIRCLE ( 'NONE', #13835, 2.700000000000000178 ) ;
#8958=LINE ( 'NONE', #14689, #5519 ) ;
#8966=ORIENTED_EDGE ( 'NONE', *, *, #15267, .T. ) ;
#8994=DIRECTION ( 'NONE',  ( 0.000000000000000000, 1.000000000000000000, 0.000000000000000000 ) ) ;
#9021=ORIENTED_EDGE ( 'NONE', *, *, #7759, .F. ) ;
#9068=CIRCLE ( 'NONE', #829, 1.500000000000000000 ) ;
#9077=LINE ( 'NONE', #1817, #3784 ) ;
#9089=CARTESIAN_POINT ( 'NONE',  ( 1.560000000000000053, -0.8660254037844384856, -1.500000000000000000 ) ) ;
#9140=VERTEX_POINT ( 'NONE', #13512 ) ;
#9142=ORIENTED_EDGE ( 'NONE', *, *, #4690, .T. ) ;
#9150=DIRECTION ( 'NONE',  ( -1.000000000000000000, 0.000000000000000000, 0.000000000000000000 ) ) ;
#9161=ADVANCED_FACE ( 'NONE', ( #3279 ), #239, .T. ) ;
#9209=CARTESIAN_POINT ( 'NONE',  ( 2.750000000000000000, 0.000000000000000000, 0.000000000000000000 ) ) ;
#9257=CARTESIAN_POINT ( 'NONE',  ( 2.426025403784448642, 0.000000000000000000, 2.168404344971008868E-16 ) ) ;
#9258=CARTESIAN_POINT ( 'NONE',  ( 22.30499999999999972, 0.000000000000000000, 2.500000000000000888 ) ) ;
#9262=CIRCLE ( 'NONE', #11697, 2.700000000000000178 ) ;
#9276=VECTOR ( 'NONE', #15516, 1000.000000000000000 ) ;
#9291=( NAMED_UNIT ( * ) SI_UNIT ( $, .STERADIAN. ) SOLID_ANGLE_UNIT ( ) );
#9302=ORIENTED_EDGE ( 'NONE', *, *, #3221, .T. ) ;
#9304=EDGE_LOOP ( 'NONE', ( #551, #11456, #12534, #14043, #2449 ) ) ;
#9307=ORIENTED_EDGE ( 'NONE', *, *, #6340, .T. ) ;
#9344=PLANE ( 'NONE',  #17743 ) ;
#9348=DIRECTION ( 'NONE',  ( 0.000000000000000000, 0.000000000000000000, 1.000000000000000000 ) ) ;
#9375=CARTESIAN_POINT ( 'NONE',  ( 2.369999999999999662, 5.817072295949927426E-16, -4.750000000000000000 ) ) ;
#9410=SURFACE_SIDE_STYLE ('',( #2409 ) ) ;
#9454=AXIS2_PLACEMENT_3D ( 'NONE', #4465, #10194, #4659 ) ;
#9497=AXIS2_PLACEMENT_3D ( 'NONE', #6972, #17269, #7153 ) ;
#9526=VECTOR ( 'NONE', #16753, 1000.000000000000000 ) ;
#9537=CIRCLE ( 'NONE', #4962, 0.2000000000000000944 ) ;
#9564=VECTOR ( 'NONE', #2667, 1000.000000000000114 ) ;
#9645=PRODUCT_DEFINITION ( 'UNKNOWN', '', #12938, #1986 ) ;
#9694=CARTESIAN_POINT ( 'NONE',  ( 0.000000000000000000, -1.732050807568877859, -1.752539433813135784E-17 ) ) ;
#9735=DIRECTION ( 'NONE',  ( 0.000000000000000000, 0.000000000000000000, 1.000000000000000000 ) ) ;
#9747=CARTESIAN_POINT ( 'NONE',  ( 1.560000000000000053, 0.000000000000000000, 2.999999999999998668 ) ) ;
#9763=CARTESIAN_POINT ( 'NONE',  ( 1.560000000000000053, -0.8660254037844384856, -1.500000000000000000 ) ) ;
#9788=CARTESIAN_POINT ( 'NONE',  ( 2.750000000000000000, 5.817072295949927426E-16, -4.750000000000000000 ) ) ;
#9789=CARTESIAN_POINT ( 'NONE',  ( 1.560000000000000053, 0.8660254037844389297, 1.500000000000000000 ) ) ;
#9797=ADVANCED_FACE ( 'NONE', ( #15574 ), #2475, .T. ) ;
#9801=CARTESIAN_POINT ( 'NONE',  ( 1.560000000000000053, 0.000000000000000000, 2.999999999999998668 ) ) ;
#9861=DIRECTION ( 'NONE',  ( 0.000000000000000000, 0.000000000000000000, 1.000000000000000000 ) ) ;
#9868=AXIS2_PLACEMENT_3D ( 'NONE', #8949, #14776, #11919 ) ;
#9877=EDGE_CURVE ( 'NONE', #10910, #14456, #12986, .T. ) ;
#9932=PLANE ( 'NONE',  #14970 ) ;
#9938=LINE ( 'NONE', #8513, #9564 ) ;
#9971=ORIENTED_EDGE ( 'NONE', *, *, #12248, .F. ) ;
#9982=VECTOR ( 'NONE', #13404, 1000.000000000000114 ) ;
#10005=PLANE ( 'NONE',  #179 ) ;
#10020=CARTESIAN_POINT ( 'NONE',  ( 1.560000000000000053, 0.000000000000000000, 0.000000000000000000 ) ) ;
#10044=LINE ( 'NONE', #8426, #772 ) ;
#10056=ORIENTED_EDGE ( 'NONE', *, *, #6707, .T. ) ;
#10059=ORIENTED_EDGE ( 'NONE', *, *, #15270, .F. ) ;
#10064=ORIENTED_EDGE ( 'NONE', *, *, #2226, .F. ) ;
#10105=DIRECTION ( 'NONE',  ( -1.000000000000000000, 0.000000000000000000, -0.000000000000000000 ) ) ;
#10123=VERTEX_POINT ( 'NONE', #2891 ) ;
#10131=ADVANCED_FACE ( 'NONE', ( #4442 ), #14756, .T. ) ;
#10133=ORIENTED_EDGE ( 'NONE', *, *, #6707, .F. ) ;
#10143=CARTESIAN_POINT ( 'NONE',  ( 4.755015822784811164, -4.336808689942017736E-16, 0.000000000000000000 ) ) ;
#10152=FACE_OUTER_BOUND ( 'NONE', #5552, .T. ) ;
#10194=DIRECTION ( 'NONE',  ( 0.000000000000000000, 0.000000000000000000, 1.000000000000000000 ) ) ;
#10196=CARTESIAN_POINT ( 'NONE',  ( 0.000000000000000000, -0.8660254037844384856, 1.500000000000000000 ) ) ;
#10210=AXIS2_PLACEMENT_3D ( 'NONE', #13106, #5733, #13194 ) ;
#10243=VERTEX_POINT ( 'NONE', #338 ) ;
#10244=DIRECTION ( 'NONE',  ( 0.000000000000000000, 0.8660254037844384856, -0.5000000000000004441 ) ) ;
#10271=DIRECTION ( 'NONE',  ( 0.000000000000000000, 0.000000000000000000, 1.000000000000000000 ) ) ;
#10272=CYLINDRICAL_SURFACE ( 'NONE', #3762, 2.500000000000000000 ) ;
#10287=CONICAL_SURFACE ( 'NONE', #15186, 2.055000000000000160, 0.7853981633974482790 ) ;
#10357=CARTESIAN_POINT ( 'NONE',  ( 2.949999999999999734, 3.061616997868383141E-16, -2.500000000000000000 ) ) ;
#10405=CIRCLE ( 'NONE', #11035, 4.750000000000000000 ) ;
#10452=ORIENTED_EDGE ( 'NONE', *, *, #9877, .T. ) ;
#10467=DIRECTION ( 'NONE',  ( -1.000000000000000000, -0.000000000000000000, -0.000000000000000000 ) ) ;
#10476=ORIENTED_EDGE ( 'NONE', *, *, #15428, .F. ) ;
#10521=ORIENTED_EDGE ( 'NONE', *, *, #12297, .T. ) ;
#10542=VERTEX_POINT ( 'NONE', #14037 ) ;
#10568=ADVANCED_FACE ( 'NONE', ( #5509 ), #4669, .T. ) ;
#10586=DIRECTION ( 'NONE',  ( -1.000000000000000000, -0.000000000000000000, -0.000000000000000000 ) ) ;
#10641=SHAPE_REPRESENTATION_RELATIONSHIP ( 'NONE' , 'NONE' ,  #6437, #14891 ) ;
#10674=VECTOR ( 'NONE', #14138, 1000.000000000000000 ) ;
#10692=CARTESIAN_POINT ( 'NONE',  ( 22.75000000000000000, 0.000000000000000000, 0.000000000000000000 ) ) ;
#10718=ORIENTED_EDGE ( 'NONE', *, *, #6340, .F. ) ;
#10742=VERTEX_POINT ( 'NONE', #17670 ) ;
#10743=EDGE_LOOP ( 'NONE', ( #9302, #8427, #12575, #10521, #4774, #3698 ) ) ;
#10794=DIRECTION ( 'NONE',  ( 0.000000000000000000, 0.000000000000000000, 1.000000000000000000 ) ) ;
#10835=DIRECTION ( 'NONE',  ( -0.000000000000000000, 0.5000000000000003331, -0.8660254037844384856 ) ) ;
#10851=FILL_AREA_STYLE_COLOUR ( '', #3636 ) ;
#10879=ORIENTED_EDGE ( 'NONE', *, *, #3522, .F. ) ;
#10895=EDGE_CURVE ( 'NONE', #13902, #10123, #14436, .T. ) ;
#10908=DIRECTION ( 'NONE',  ( -1.000000000000000000, -0.000000000000000000, -0.000000000000000000 ) ) ;
#10910=VERTEX_POINT ( 'NONE', #9788 ) ;
#10999=CARTESIAN_POINT ( 'NONE',  ( 2.369999999999999662, 0.000000000000000000, 0.000000000000000000 ) ) ;
#11035=AXIS2_PLACEMENT_3D ( 'NONE', #10999, #10908, #3629 ) ;
#11070=ADVANCED_FACE ( 'NONE', ( #16303 ), #10272, .T. ) ;
#11091=FACE_OUTER_BOUND ( 'NONE', #15139, .T. ) ;
#11095=DIRECTION ( 'NONE',  ( -1.000000000000000000, 0.000000000000000000, 0.000000000000000000 ) ) ;
#11104=PLANE ( 'NONE',  #7945 ) ;
#11191=DIRECTION ( 'NONE',  ( -1.000000000000000000, 0.000000000000000000, 0.000000000000000000 ) ) ;
#11210=DIRECTION ( 'NONE',  ( -0.000000000000000000, 0.000000000000000000, 1.000000000000000000 ) ) ;
#11224=LINE ( 'NONE', #9763, #17825 ) ;
#11248=DIRECTION ( 'NONE',  ( 0.000000000000000000, 0.000000000000000000, 1.000000000000000000 ) ) ;
#11265=PLANE ( 'NONE',  #5069 ) ;
#11288=CARTESIAN_POINT ( 'NONE',  ( 2.750000000000000000, 0.000000000000000000, 0.000000000000000000 ) ) ;
#11308=ORIENTED_EDGE ( 'NONE', *, *, #10895, .F. ) ;
#11330=CARTESIAN_POINT ( 'NONE',  ( 2.949999999999999734, 0.000000000000000000, 2.700000000000000178 ) ) ;
#11361=CARTESIAN_POINT ( 'NONE',  ( 22.75000000000000000, 0.000000000000000000, 0.000000000000000000 ) ) ;
#11370=AXIS2_PLACEMENT_3D ( 'NONE', #14849, #14746, #13317 ) ;
#11414=EDGE_LOOP ( 'NONE', ( #7468, #4293, #2171, #8340 ) ) ;
#11431=DIRECTION ( 'NONE',  ( 0.000000000000000000, 0.000000000000000000, 1.000000000000000000 ) ) ;
#11451=PLANE ( 'NONE',  #9497 ) ;
#11456=ORIENTED_EDGE ( 'NONE', *, *, #4966, .T. ) ;
#11459=ADVANCED_FACE ( 'NONE', ( #11595 ), #7299, .T. ) ;
#11460=ADVANCED_FACE ( 'NONE', ( #10152 ), #5840, .T. ) ;
#11466=DIRECTION ( 'NONE',  ( -0.000000000000000000, -0.5000000000000004441, 0.8660254037844383745 ) ) ;
#11476=CARTESIAN_POINT ( 'NONE',  ( 0.000000000000000000, 5.817072295949927426E-16, -4.750000000000000000 ) ) ;
#11487=COLOUR_RGB ( '', 0.09019608, 0.27058824, 0.51372549) ;
#11508=AXIS2_PLACEMENT_3D ( 'NONE', #17114, #15672, #11210 ) ;
#11518=DIRECTION ( 'NONE',  ( 0.000000000000000000, -1.000000000000000000, 0.000000000000000000 ) ) ;
#11595=FACE_OUTER_BOUND ( 'NONE', #367, .T. ) ;
#11649=CARTESIAN_POINT ( 'NONE',  ( 4.755015822784811164, -4.336808689942017736E-16, 0.000000000000000000 ) ) ;
#11660=DIRECTION ( 'NONE',  ( -1.000000000000000000, -0.000000000000000000, -0.000000000000000000 ) ) ;
#11684=FACE_BOUND ( 'NONE', #4890, .T. ) ;
#11697=AXIS2_PLACEMENT_3D ( 'NONE', #14428, #4394, #5915 ) ;
#11722=EDGE_CURVE ( 'NONE', #18645, #18680, #9938, .T. ) ;
#11749=LINE ( 'NONE', #9257, #15088 ) ;
#11766=ORIENTED_EDGE ( 'NONE', *, *, #3647, .F. ) ;
#11782=EDGE_CURVE ( 'NONE', #5854, #16571, #9262, .T. ) ;
#11789=ORIENTED_EDGE ( 'NONE', *, *, #15319, .F. ) ;
#11799=LINE ( 'NONE', #11895, #7014 ) ;
#11818=ORIENTED_EDGE ( 'NONE', *, *, #12847, .F. ) ;
#11825=CARTESIAN_POINT ( 'NONE',  ( 2.369999999999999662, 0.000000000000000000, 0.000000000000000000 ) ) ;
#11855=AXIS2_PLACEMENT_3D ( 'NONE', #18370, #5458, #17120 ) ;
#11895=CARTESIAN_POINT ( 'NONE',  ( 1.560000000000000053, 0.8660254037844389297, 1.500000000000000000 ) ) ;
#11897=DIRECTION ( 'NONE',  ( -1.000000000000000000, -0.000000000000000000, -0.000000000000000000 ) ) ;
#11919=DIRECTION ( 'NONE',  ( 0.000000000000000000, 0.000000000000000000, 1.000000000000000000 ) ) ;
#11928=VERTEX_POINT ( 'NONE', #16796 ) ;
#11979=ORIENTED_EDGE ( 'NONE', *, *, #6371, .T. ) ;
#11990=ORIENTED_EDGE ( 'NONE', *, *, #10895, .T. ) ;
#12169=SURFACE_STYLE_FILL_AREA ( #14928 ) ;
#12174=CARTESIAN_POINT ( 'NONE',  ( 1.560000000000000053, 0.000000000000000000, 0.000000000000000000 ) ) ;
#12223=ORIENTED_EDGE ( 'NONE', *, *, #13469, .T. ) ;
#12248=EDGE_CURVE ( 'NONE', #8289, #11928, #6819, .T. ) ;
#12270=EDGE_LOOP ( 'NONE', ( #11789, #8560, #2266, #13793 ) ) ;
#12297=EDGE_CURVE ( 'NONE', #7502, #10742, #12554, .T. ) ;
#12344=PRESENTATION_STYLE_ASSIGNMENT (( #1845 ) ) ;
#12349=LINE ( 'NONE', #17911, #1758 ) ;
#12359=AXIS2_PLACEMENT_3D ( 'NONE', #18628, #5622, #14522 ) ;
#12360=VERTEX_POINT ( 'NONE', #15796 ) ;
#12429=AXIS2_PLACEMENT_3D ( 'NONE', #18479, #18658, #9861 ) ;
#12478=CARTESIAN_POINT ( 'NONE',  ( -997.5739745962155212, 0.000000000000000000, 0.000000000000000000 ) ) ;
#12534=ORIENTED_EDGE ( 'NONE', *, *, #6952, .T. ) ;
#12554=LINE ( 'NONE', #5293, #9276 ) ;
#12575=ORIENTED_EDGE ( 'NONE', *, *, #15429, .T. ) ;
#12576=ORIENTED_EDGE ( 'NONE', *, *, #6371, .F. ) ;
#12594=CARTESIAN_POINT ( 'NONE',  ( 22.75000000000000000, 0.000000000000000000, 0.000000000000000000 ) ) ;
#12619=FACE_OUTER_BOUND ( 'NONE', #17651, .T. ) ;
#12631=SURFACE_STYLE_USAGE ( .BOTH. , #9410 ) ;
#12671=ORIENTED_EDGE ( 'NONE', *, *, #773, .F. ) ;
#12732=CARTESIAN_POINT ( 'NONE',  ( 1.560000000000000053, 1.299038105676658228, 0.7500000000000009992 ) ) ;
#12781=CARTESIAN_POINT ( 'NONE',  ( 2.426025403784448642, 2.168404344971008868E-16, 0.000000000000000000 ) ) ;
#12806=LINE ( 'NONE', #11476, #768 ) ;
#12813=DIRECTION ( 'NONE',  ( 0.000000000000000000, -0.8660254037844384856, 0.5000000000000004441 ) ) ;
#12827=EDGE_CURVE ( 'NONE', #16571, #102, #2759, .T. ) ;
#12837=ORIENTED_EDGE ( 'NONE', *, *, #1515, .T. ) ;
#12847=EDGE_CURVE ( 'NONE', #14456, #10910, #18632, .T. ) ;
#12866=CARTESIAN_POINT ( 'NONE',  ( 0.000000000000000000, -1.732050807568877859, -1.752539433813135784E-17 ) ) ;
#12869=FACE_OUTER_BOUND ( 'NONE', #7785, .T. ) ;
#12893=LINE ( 'NONE', #18718, #17406 ) ;
#12922=DIRECTION ( 'NONE',  ( -1.000000000000000000, 0.000000000000000000, 0.000000000000000000 ) ) ;
#12926=LINE ( 'NONE', #9694, #15767 ) ;
#12930=ORIENTED_EDGE ( 'NONE', *, *, #160, .F. ) ;
#12938=PRODUCT_DEFINITION_FORMATION_WITH_SPECIFIED_SOURCE ( 'ANY', '', #15013, .NOT_KNOWN. ) ;
#12983=EDGE_LOOP ( 'NONE', ( #17213, #13498, #2402, #3440, #227 ) ) ;
#12986=CIRCLE ( 'NONE', #16366, 4.750000000000000000 ) ;
#13048=UNCERTAINTY_MEASURE_WITH_UNIT (LENGTH_MEASURE( 1.000000000000000082E-05 ), #18467, 'distance_accuracy_value', 'NONE');
#13053=ORIENTED_EDGE ( 'NONE', *, *, #3522, .T. ) ;
#13106=CARTESIAN_POINT ( 'NONE',  ( 1.560000000000000053, 0.000000000000000000, 2.999999999999998668 ) ) ;
#13132=DIRECTION ( 'NONE',  ( -0.000000000000000000, -0.5000000000000004441, 0.8660254037844383745 ) ) ;
#13137=CARTESIAN_POINT ( 'NONE',  ( 0.000000000000000000, 0.000000000000000000, 0.000000000000000000 ) ) ;
#13179=ADVANCED_FACE ( 'NONE', ( #360 ), #9344, .T. ) ;
#13187=DIRECTION ( 'NONE',  ( -1.000000000000000000, 0.000000000000000000, 0.000000000000000000 ) ) ;
#13194=DIRECTION ( 'NONE',  ( 0.000000000000000000, 0.000000000000000000, 1.000000000000000000 ) ) ;
#13244=DIRECTION ( 'NONE',  ( -0.000000000000000000, 1.000000000000000000, -0.000000000000000000 ) ) ;
#13265=DIRECTION ( 'NONE',  ( -0.000000000000000000, -1.000000000000000000, -0.000000000000000000 ) ) ;
#13269=EDGE_CURVE ( 'NONE', #15874, #15040, #10405, .T. ) ;
#13271=ORIENTED_EDGE ( 'NONE', *, *, #7420, .T. ) ;
#13274=DIRECTION ( 'NONE',  ( -0.000000000000000000, 0.5000000000000004441, 0.8660254037844383745 ) ) ;
#13308=FACE_OUTER_BOUND ( 'NONE', #1172, .T. ) ;
#13317=DIRECTION ( 'NONE',  ( 0.000000000000000000, 0.000000000000000000, 1.000000000000000000 ) ) ;
#13330=VECTOR ( 'NONE', #13187, 1000.000000000000000 ) ;
#13340=ORIENTED_EDGE ( 'NONE', *, *, #13269, .T. ) ;
#13351=AXIS2_PLACEMENT_3D ( 'NONE', #12174, #18186, #5085 ) ;
#13386=FACE_OUTER_BOUND ( 'NONE', #8877, .T. ) ;
#13404=DIRECTION ( 'NONE',  ( -0.7071067811865474617, 8.659560562354932858E-17, -0.7071067811865474617 ) ) ;
#13410=ORIENTED_EDGE ( 'NONE', *, *, #16604, .F. ) ;
#13417=EDGE_LOOP ( 'NONE', ( #7337, #10452, #6151, #8257, #15379 ) ) ;
#13418=ADVANCED_FACE ( 'NONE', ( #1126 ), #11451, .T. ) ;
#13437=LINE ( 'NONE', #17752, #6270 ) ;
#13449=CARTESIAN_POINT ( 'NONE',  ( 1.560000000000000053, 0.000000000000000000, -1.499999999999999556 ) ) ;
#13455=VERTEX_POINT ( 'NONE', #4761 ) ;
#13468=CARTESIAN_POINT ( 'NONE',  ( 1.560000000000000053, 1.732050807568878747, 7.017607234860990640E-28 ) ) ;
#13469=EDGE_CURVE ( 'NONE', #6435, #18680, #8958, .T. ) ;
#13498=ORIENTED_EDGE ( 'NONE', *, *, #18211, .T. ) ;
#13512=CARTESIAN_POINT ( 'NONE',  ( 1.560000000000000053, 1.299038105676658228, -0.7500000000000009992 ) ) ;
#13524=CARTESIAN_POINT ( 'NONE',  ( 22.75000000000000000, 0.000000000000000000, 0.000000000000000000 ) ) ;
#13568=DIRECTION ( 'NONE',  ( -1.000000000000000000, -0.000000000000000000, -0.000000000000000000 ) ) ;
#13677=CARTESIAN_POINT ( 'NONE',  ( 2.750000000000000000, 0.000000000000000000, 0.000000000000000000 ) ) ;
#13701=CARTESIAN_POINT ( 'NONE',  ( 1.560000000000000053, 1.732050807568878747, 7.017607234860990640E-28 ) ) ;
#13786=DIRECTION ( 'NONE',  ( -0.000000000000000000, 0.5000000000000004441, 0.8660254037844383745 ) ) ;
#13793=ORIENTED_EDGE ( 'NONE', *, *, #388, .F. ) ;
#13827=VERTEX_POINT ( 'NONE', #9789 ) ;
#13835=AXIS2_PLACEMENT_3D ( 'NONE', #9209, #16488, #1859 ) ;
#13838=VERTEX_POINT ( 'NONE', #8842 ) ;
#13848=DIRECTION ( 'NONE',  ( -1.000000000000000000, -0.000000000000000000, -0.000000000000000000 ) ) ;
#13867=( NAMED_UNIT ( * ) PLANE_ANGLE_UNIT ( ) SI_UNIT ( $, .RADIAN. ) );
#13875=CARTESIAN_POINT ( 'NONE',  ( 1.560000000000000053, -1.732050807568877859, -1.752539433813135784E-17 ) ) ;
#13900=FACE_OUTER_BOUND ( 'NONE', #17076, .T. ) ;
#13902=VERTEX_POINT ( 'NONE', #7228 ) ;
#13931=DIRECTION ( 'NONE',  ( -1.000000000000000000, 0.000000000000000000, 0.000000000000000000 ) ) ;
#13938=MECHANICAL_DESIGN_GEOMETRIC_PRESENTATION_REPRESENTATION('',(#3857),#217);
#13948=ORIENTED_EDGE ( 'NONE', *, *, #15267, .F. ) ;
#13984=PRESENTATION_STYLE_ASSIGNMENT (( #12631 ) ) ;
#13994=DIRECTION ( 'NONE',  ( -0.000000000000000000, -0.5000000000000003331, -0.8660254037844384856 ) ) ;
#14018=VECTOR ( 'NONE', #2729, 1000.000000000000000 ) ;
#14037=CARTESIAN_POINT ( 'NONE',  ( 0.000000000000000000, -2.375000000000000444, -4.362804221962445569E-16 ) ) ;
#14043=ORIENTED_EDGE ( 'NONE', *, *, #7573, .T. ) ;
#14087=DIRECTION ( 'NONE',  ( -1.000000000000000000, -0.000000000000000000, -0.000000000000000000 ) ) ;
#14092=ORIENTED_EDGE ( 'NONE', *, *, #5974, .F. ) ;
#14138=DIRECTION ( 'NONE',  ( -1.000000000000000000, -0.000000000000000000, -0.000000000000000000 ) ) ;
#14200=DIRECTION ( 'NONE',  ( 1.000000000000000000, 0.000000000000000000, 0.000000000000000000 ) ) ;
#14297=DIRECTION ( 'NONE',  ( 0.000000000000000000, 0.000000000000000000, 1.000000000000000000 ) ) ;
#14315=STYLED_ITEM ( 'NONE', ( #13984 ), #16760 ) ;
#14320=DIRECTION ( 'NONE',  ( -0.000000000000000000, -1.000000000000000000, -0.000000000000000000 ) ) ;
#14335=DIRECTION ( 'NONE',  ( -1.000000000000000000, 0.000000000000000000, -0.000000000000000000 ) ) ;
#14348=SPHERICAL_SURFACE ( 'NONE', #5329, 5.315148208181397216 ) ;
#14383=ADVANCED_FACE ( 'NONE', ( #11091 ), #1157, .F. ) ;
#14395=ORIENTED_EDGE ( 'NONE', *, *, #1515, .F. ) ;
#14399=DIRECTION ( 'NONE',  ( -0.000000000000000000, 0.000000000000000000, 1.000000000000000000 ) ) ;
#14428=CARTESIAN_POINT ( 'NONE',  ( 2.750000000000000000, 0.000000000000000000, 0.000000000000000000 ) ) ;
#14433=PLANE ( 'NONE',  #11508 ) ;
#14436=CIRCLE ( 'NONE', #409, 2.055000000000000160 ) ;
#14456=VERTEX_POINT ( 'NONE', #8308 ) ;
#14522=DIRECTION ( 'NONE',  ( 0.000000000000000000, 0.000000000000000000, 1.000000000000000000 ) ) ;
#14530=EDGE_CURVE ( 'NONE', #13827, #2439, #18609, .T. ) ;
#14605=LINE ( 'NONE', #1523, #6861 ) ;
#14689=CARTESIAN_POINT ( 'NONE',  ( 1.560000000000000053, 0.8660254037844389297, -1.500000000000000000 ) ) ;
#14691=ORIENTED_EDGE ( 'NONE', *, *, #7100, .F. ) ;
#14746=DIRECTION ( 'NONE',  ( -1.000000000000000000, -0.000000000000000000, -0.000000000000000000 ) ) ;
#14756=CYLINDRICAL_SURFACE ( 'NONE', #18784, 2.500000000000000000 ) ;
#14759=EDGE_CURVE ( 'NONE', #102, #18437, #18512, .T. ) ;
#14775=LINE ( 'NONE', #3305, #7482 ) ;
#14776=DIRECTION ( 'NONE',  ( -1.000000000000000000, -0.000000000000000000, -0.000000000000000000 ) ) ;
#14786=EDGE_CURVE ( 'NONE', #13455, #15874, #2347, .T. ) ;
#14791=CIRCLE ( 'NONE', #7175, 4.750000000000000000 ) ;
#14796=CIRCLE ( 'NONE', #15108, 1.500000000000000000 ) ;
#14812=EDGE_LOOP ( 'NONE', ( #579, #13340, #16008, #5065, #2584 ) ) ;
#14828=CARTESIAN_POINT ( 'NONE',  ( 0.000000000000000000, 0.000000000000000000, 2.500000000000000000 ) ) ;
#14833=CARTESIAN_POINT ( 'NONE',  ( 2.949999999999999734, 0.000000000000000000, 0.000000000000000000 ) ) ;
#14849=CARTESIAN_POINT ( 'NONE',  ( 22.75000000000000000, 0.000000000000000000, 0.000000000000000000 ) ) ;
#14863=EDGE_CURVE ( 'NONE', #18437, #102, #1439, .T. ) ;
#14891=ADVANCED_BREP_SHAPE_REPRESENTATION ( '', ( #16760, #2030 ), #809 ) ;
#14911=CARTESIAN_POINT ( 'NONE',  ( 2.949999999999999734, 3.306546357697853733E-16, -2.700000000000000178 ) ) ;
#14928=FILL_AREA_STYLE ('',( #2133 ) ) ;
#14941=ORIENTED_EDGE ( 'NONE', *, *, #8087, .F. ) ;
#14970=AXIS2_PLACEMENT_3D ( 'NONE', #15761, #1237, #14335 ) ;
#14973=DIRECTION ( 'NONE',  ( 0.000000000000000000, 0.000000000000000000, 1.000000000000000000 ) ) ;
#14987=DIRECTION ( 'NONE',  ( -1.000000000000000000, -0.000000000000000000, -0.000000000000000000 ) ) ;
#15013=PRODUCT ( 'socket button head screw_iso_ISO 7380 - M5 x 20 - 20C', 'socket button head screw_iso_ISO 7380 - M5 x 20 - 20C', '', ( #8266 ) ) ;
#15040=VERTEX_POINT ( 'NONE', #15155 ) ;
#15054=FACE_OUTER_BOUND ( 'NONE', #12270, .T. ) ;
#15088=VECTOR ( 'NONE', #7844, 1000.000000000000114 ) ;
#15089=LINE ( 'NONE', #6304, #16928 ) ;
#15108=AXIS2_PLACEMENT_3D ( 'NONE', #10020, #8322, #15855 ) ;
#15139=EDGE_LOOP ( 'NONE', ( #2437, #7982, #18715, #417 ) ) ;
#15155=CARTESIAN_POINT ( 'NONE',  ( 2.369999999999999662, -4.750000000000000888, -5.817072295949926440E-16 ) ) ;
#15186=AXIS2_PLACEMENT_3D ( 'NONE', #13524, #7814, #17744 ) ;
#15208=FACE_OUTER_BOUND ( 'NONE', #9304, .T. ) ;
#15209=VECTOR ( 'NONE', #14320, 1000.000000000000000 ) ;
#15210=ORIENTED_EDGE ( 'NONE', *, *, #15319, .T. ) ;
#15219=EDGE_CURVE ( 'NONE', #12360, #4507, #12926, .T. ) ;
#15235=DIRECTION ( 'NONE',  ( -1.000000000000000000, -0.000000000000000000, -0.000000000000000000 ) ) ;
#15267=EDGE_CURVE ( 'NONE', #10542, #6415, #1744, .T. ) ;
#15270=EDGE_CURVE ( 'NONE', #3148, #3596, #9068, .T. ) ;
#15300=DIRECTION ( 'NONE',  ( -1.000000000000000000, 0.000000000000000000, 0.000000000000000000 ) ) ;
#15319=EDGE_CURVE ( 'NONE', #10123, #11928, #2972, .T. ) ;
#15334=VECTOR ( 'NONE', #5756, 1000.000000000000114 ) ;
#15355=EDGE_LOOP ( 'NONE', ( #16579, #6392, #17160, #17973, #10133 ) ) ;
#15369=ADVANCED_FACE ( 'NONE', ( #11684, #13308 ), #1556, .F. ) ;
#15379=ORIENTED_EDGE ( 'NONE', *, *, #13269, .F. ) ;
#15406=ORIENTED_EDGE ( 'NONE', *, *, #5540, .T. ) ;
#15422=ORIENTED_EDGE ( 'NONE', *, *, #17300, .T. ) ;
#15428=EDGE_CURVE ( 'NONE', #9140, #18680, #18237, .T. ) ;
#15429=EDGE_CURVE ( 'NONE', #4507, #7502, #12349, .T. ) ;
#15504=EDGE_LOOP ( 'NONE', ( #2851, #13271, #9307, #1952, #13410 ) ) ;
#15516=DIRECTION ( 'NONE',  ( -0.000000000000000000, 1.000000000000000000, -0.000000000000000000 ) ) ;
#15533=MECHANICAL_DESIGN_GEOMETRIC_PRESENTATION_REPRESENTATION('',(#14315),#892);
#15536=DIRECTION ( 'NONE',  ( 0.000000000000000000, 0.000000000000000000, 1.000000000000000000 ) ) ;
#15574=FACE_OUTER_BOUND ( 'NONE', #12983, .T. ) ;
#15586=CARTESIAN_POINT ( 'NONE',  ( 2.750000000000000000, 3.306546357697853733E-16, -2.700000000000000178 ) ) ;
#15601=SHAPE_DEFINITION_REPRESENTATION ( #5829, #6437 ) ;
#15623=ORIENTED_EDGE ( 'NONE', *, *, #8017, .T. ) ;
#15628=ORIENTED_EDGE ( 'NONE', *, *, #12248, .T. ) ;
#15670=ORIENTED_EDGE ( 'NONE', *, *, #4025, .F. ) ;
#15672=DIRECTION ( 'NONE',  ( -1.000000000000000000, 0.000000000000000000, -0.000000000000000000 ) ) ;
#15716=CARTESIAN_POINT ( 'NONE',  ( 0.000000000000000000, 0.000000000000000000, 0.000000000000000000 ) ) ;
#15754=CARTESIAN_POINT ( 'NONE',  ( 0.000000000000000000, -0.8660254037844384856, -1.500000000000000000 ) ) ;
#15761=CARTESIAN_POINT ( 'NONE',  ( 1.560000000000000053, -0.8660254037844384856, 1.500000000000000000 ) ) ;
#15766=AXIS2_PLACEMENT_3D ( 'NONE', #17180, #17009, #9735 ) ;
#15767=VECTOR ( 'NONE', #13994, 1000.000000000000114 ) ;
#15768=CONICAL_SURFACE ( 'NONE', #1730, 1732.050807568857181, 1.047197551196592746 ) ;
#15784=FACE_OUTER_BOUND ( 'NONE', #15504, .T. ) ;
#15796=CARTESIAN_POINT ( 'NONE',  ( 0.000000000000000000, -0.8660254037844384856, 1.500000000000000000 ) ) ;
#15806=AXIS2_PLACEMENT_3D ( 'NONE', #14833, #13848, #18424 ) ;
#15817=ADVANCED_FACE ( 'NONE', ( #15208 ), #15768, .F. ) ;
#15839=DIRECTION ( 'NONE',  ( -1.000000000000000000, -0.000000000000000000, -0.000000000000000000 ) ) ;
#15852=ADVANCED_FACE ( 'NONE', ( #13386 ), #6419, .T. ) ;
#15855=DIRECTION ( 'NONE',  ( 0.000000000000000000, 0.000000000000000000, 1.000000000000000000 ) ) ;
#15874=VERTEX_POINT ( 'NONE', #9375 ) ;
#15909=EDGE_CURVE ( 'NONE', #3148, #6435, #6132, .T. ) ;
#15964=DIRECTION ( 'NONE',  ( 0.000000000000000000, -0.5000000000000003331, -0.8660254037844383745 ) ) ;
#16008=ORIENTED_EDGE ( 'NONE', *, *, #4025, .T. ) ;
#16083=AXIS2_PLACEMENT_3D ( 'NONE', #1636, #10244, #5832 ) ;
#16088=AXIS2_PLACEMENT_3D ( 'NONE', #8271, #14087, #2241 ) ;
#16105=UNCERTAINTY_MEASURE_WITH_UNIT (LENGTH_MEASURE( 1.000000000000000082E-05 ), #3649, 'distance_accuracy_value', 'NONE');
#16117=VERTEX_POINT ( 'NONE', #7160 ) ;
#16142=ADVANCED_FACE ( 'NONE', ( #13900 ), #18226, .F. ) ;
#16303=FACE_OUTER_BOUND ( 'NONE', #4073, .T. ) ;
#16366=AXIS2_PLACEMENT_3D ( 'NONE', #11288, #15235, #5525 ) ;
#16385=ORIENTED_EDGE ( 'NONE', *, *, #17542, .T. ) ;
#16412=CLOSED_SHELL ( 'NONE', ( #17664, #16142, #10568, #11070, #9797, #7453, #5370, #6747, #9161, #15369, #10131, #5835, #18572, #14383, #1567, #15852, #13418, #6466, #11460, #17299, #11459, #3951, #8542, #6701, #13179, #7474, #15817 ) ) ;
#16467=LINE ( 'NONE', #14828, #10674 ) ;
#16472=AXIS2_PLACEMENT_3D ( 'NONE', #960, #17387, #2838 ) ;
#16488=DIRECTION ( 'NONE',  ( -1.000000000000000000, -0.000000000000000000, -0.000000000000000000 ) ) ;
#16505=DIRECTION ( 'NONE',  ( 0.000000000000000000, 0.000000000000000000, 1.000000000000000000 ) ) ;
#16521=DIRECTION ( 'NONE',  ( -1.000000000000000000, -0.000000000000000000, -0.000000000000000000 ) ) ;
#16571=VERTEX_POINT ( 'NONE', #15586 ) ;
#16579=ORIENTED_EDGE ( 'NONE', *, *, #14530, .T. ) ;
#16598=VERTEX_POINT ( 'NONE', #18454 ) ;
#16604=EDGE_CURVE ( 'NONE', #16598, #12360, #1480, .T. ) ;
#16612=CARTESIAN_POINT ( 'NONE',  ( 2.949999999999999734, 0.000000000000000000, 0.000000000000000000 ) ) ;
#16701=AXIS2_PLACEMENT_3D ( 'NONE', #9089, #496, #3541 ) ;
#16753=DIRECTION ( 'NONE',  ( -1.000000000000000000, 0.000000000000000000, 0.000000000000000000 ) ) ;
#16760=MANIFOLD_SOLID_BREP ( 'Hex', #16412 ) ;
#16796=CARTESIAN_POINT ( 'NONE',  ( 22.30499999999999972, 3.061616997868384620E-16, -2.500000000000001332 ) ) ;
#16819=APPLICATION_CONTEXT ( 'automotive_design' ) ;
#16825=LINE ( 'NONE', #8588, #1824 ) ;
#16913=DIRECTION ( 'NONE',  ( 0.000000000000000000, 0.000000000000000000, 1.000000000000000000 ) ) ;
#16928=VECTOR ( 'NONE', #2008, 1000.000000000000000 ) ;
#17009=DIRECTION ( 'NONE',  ( -1.000000000000000000, -0.000000000000000000, -0.000000000000000000 ) ) ;
#17072=ORIENTED_EDGE ( 'NONE', *, *, #9877, .F. ) ;
#17076=EDGE_LOOP ( 'NONE', ( #12930, #3472, #7835, #14691 ) ) ;
#17114=CARTESIAN_POINT ( 'NONE',  ( 0.000000000000000000, 0.000000000000000000, 0.000000000000000000 ) ) ;
#17117=CARTESIAN_POINT ( 'NONE',  ( 0.000000000000000000, 2.375000000000000444, 0.000000000000000000 ) ) ;
#17120=DIRECTION ( 'NONE',  ( 0.000000000000000000, 0.000000000000000000, 1.000000000000000000 ) ) ;
#17160=ORIENTED_EDGE ( 'NONE', *, *, #16604, .T. ) ;
#17180=CARTESIAN_POINT ( 'NONE',  ( 2.369999999999999662, 0.000000000000000000, 0.000000000000000000 ) ) ;
#17213=ORIENTED_EDGE ( 'NONE', *, *, #12847, .T. ) ;
#17222=ORIENTED_EDGE ( 'NONE', *, *, #5774, .T. ) ;
#17249=DIRECTION ( 'NONE',  ( 1.000000000000000000, 0.000000000000000000, 0.000000000000000000 ) ) ;
#17251=DIRECTION ( 'NONE',  ( -1.000000000000000000, -0.000000000000000000, -0.000000000000000000 ) ) ;
#17266=LINE ( 'NONE', #10196, #14018 ) ;
#17269=DIRECTION ( 'NONE',  ( 0.000000000000000000, 0.000000000000000000, 1.000000000000000000 ) ) ;
#17280=ORIENTED_EDGE ( 'NONE', *, *, #773, .T. ) ;
#17294=AXIS2_PLACEMENT_3D ( 'NONE', #4266, #17251, #11431 ) ;
#17299=ADVANCED_FACE ( 'NONE', ( #4014 ), #9932, .T. ) ;
#17300=EDGE_CURVE ( 'NONE', #11928, #102, #12893, .T. ) ;
#17325=DIRECTION ( 'NONE',  ( -1.000000000000000000, -0.000000000000000000, -0.000000000000000000 ) ) ;
#17346=CARTESIAN_POINT ( 'NONE',  ( 2.949999999999999734, 0.000000000000000000, 0.000000000000000000 ) ) ;
#17370=CARTESIAN_POINT ( 'NONE',  ( 1.560000000000000053, -0.8660254037844384856, 1.500000000000000000 ) ) ;
#17377=CARTESIAN_POINT ( 'NONE',  ( 1.560000000000000053, 1.732050807568878747, 7.017607234860990640E-28 ) ) ;
#17387=DIRECTION ( 'NONE',  ( 0.000000000000000000, 1.224646799147353207E-16, -1.000000000000000000 ) ) ;
#17406=VECTOR ( 'NONE', #5619, 1000.000000000000000 ) ;
#17444=CARTESIAN_POINT ( 'NONE',  ( 0.000000000000000000, 0.000000000000000000, 0.000000000000000000 ) ) ;
#17485=DIRECTION ( 'NONE',  ( 0.000000000000000000, 0.000000000000000000, 1.000000000000000000 ) ) ;
#17495=AXIS2_PLACEMENT_3D ( 'NONE', #2777, #7394, #17510 ) ;
#17510=DIRECTION ( 'NONE',  ( 0.000000000000000000, 0.5000000000000003331, -0.8660254037844383745 ) ) ;
#17542=EDGE_CURVE ( 'NONE', #13455, #6415, #5173, .T. ) ;
#17557=DIRECTION ( 'NONE',  ( -0.7071067811865474617, 0.000000000000000000, 0.7071067811865474617 ) ) ;
#17651=EDGE_LOOP ( 'NONE', ( #9142, #8966 ) ) ;
#17664=ADVANCED_FACE ( 'NONE', ( #18127 ), #5624, .F. ) ;
#17670=CARTESIAN_POINT ( 'NONE',  ( 0.000000000000000000, 0.8660254037844389297, -1.500000000000000000 ) ) ;
#17733=DIRECTION ( 'NONE',  ( 0.000000000000000000, 0.000000000000000000, 1.000000000000000000 ) ) ;
#17736=DIRECTION ( 'NONE',  ( -1.000000000000000000, -0.000000000000000000, -0.000000000000000000 ) ) ;
#17743=AXIS2_PLACEMENT_3D ( 'NONE', #3308, #9150, #14973 ) ;
#17744=DIRECTION ( 'NONE',  ( 0.000000000000000000, 0.000000000000000000, 1.000000000000000000 ) ) ;
#17752=CARTESIAN_POINT ( 'NONE',  ( 0.000000000000000000, 0.8660254037844389297, 1.500000000000000000 ) ) ;
#17779=ORIENTED_EDGE ( 'NONE', *, *, #2332, .T. ) ;
#17801=FACE_OUTER_BOUND ( 'NONE', #1582, .T. ) ;
#17814=EDGE_LOOP ( 'NONE', ( #2719, #11979, #3467, #11766, #9021 ) ) ;
#17823=EDGE_LOOP ( 'NONE', ( #10879, #12576, #5278 ) ) ;
#17825=VECTOR ( 'NONE', #4031, 1000.000000000000114 ) ;
#17911=CARTESIAN_POINT ( 'NONE',  ( 0.000000000000000000, -0.8660254037844384856, -1.500000000000000000 ) ) ;
#17973=ORIENTED_EDGE ( 'NONE', *, *, #3221, .F. ) ;
#18127=FACE_OUTER_BOUND ( 'NONE', #5778, .T. ) ;
#18133=EDGE_CURVE ( 'NONE', #3596, #2439, #2877, .T. ) ;
#18186=DIRECTION ( 'NONE',  ( -1.000000000000000000, -0.000000000000000000, -0.000000000000000000 ) ) ;
#18205=ORIENTED_EDGE ( 'NONE', *, *, #18133, .F. ) ;
#18211=EDGE_CURVE ( 'NONE', #10910, #15874, #12806, .T. ) ;
#18222=ORIENTED_EDGE ( 'NONE', *, *, #14759, .T. ) ;
#18226=TOROIDAL_SURFACE ( 'NONE', #1745, 2.700000000000000178, 0.2000000000000000111 ) ;
#18237=CIRCLE ( 'NONE', #13351, 1.500000000000000000 ) ;
#18271=CIRCLE ( 'NONE', #11855, 2.500000000000000888 ) ;
#18370=CARTESIAN_POINT ( 'NONE',  ( 22.30499999999999972, 0.000000000000000000, 0.000000000000000000 ) ) ;
#18374=DIRECTION ( 'NONE',  ( -0.000000000000000000, 0.5000000000000004441, 0.8660254037844383745 ) ) ;
#18375=( NAMED_UNIT ( * ) PLANE_ANGLE_UNIT ( ) SI_UNIT ( $, .RADIAN. ) );
#18409=EDGE_LOOP ( 'NONE', ( #12223, #15623, #2718, #2591, #6603 ) ) ;
#18424=DIRECTION ( 'NONE',  ( 0.000000000000000000, 0.000000000000000000, 1.000000000000000000 ) ) ;
#18431=SPHERICAL_SURFACE ( 'NONE', #8902, 5.315148208181397216 ) ;
#18432=CARTESIAN_POINT ( 'NONE',  ( 1.560000000000000053, 0.8660254037844389297, 1.500000000000000000 ) ) ;
#18437=VERTEX_POINT ( 'NONE', #5243 ) ;
#18454=CARTESIAN_POINT ( 'NONE',  ( 1.560000000000000053, -0.8660254037844384856, 1.500000000000000000 ) ) ;
#18467=( LENGTH_UNIT ( ) NAMED_UNIT ( * ) SI_UNIT ( .MILLI., .METRE. ) );
#18479=CARTESIAN_POINT ( 'NONE',  ( 0.000000000000000000, 0.000000000000000000, 0.000000000000000000 ) ) ;
#18502=EDGE_LOOP ( 'NONE', ( #641, #18578, #14092 ) ) ;
#18512=CIRCLE ( 'NONE', #214, 2.500000000000000000 ) ;
#18520=DIRECTION ( 'NONE',  ( 0.000000000000000000, 0.000000000000000000, 1.000000000000000000 ) ) ;
#18553=PLANE ( 'NONE',  #6480 ) ;
#18572=ADVANCED_FACE ( 'NONE', ( #12869 ), #10005, .F. ) ;
#18578=ORIENTED_EDGE ( 'NONE', *, *, #15909, .F. ) ;
#18580=CARTESIAN_POINT ( 'NONE',  ( 1.560000000000000053, 0.000000000000000000, 1.500000000000000000 ) ) ;
#18609=LINE ( 'NONE', #17370, #15209 ) ;
#18628=CARTESIAN_POINT ( 'NONE',  ( 1.560000000000000053, 0.000000000000000000, 0.000000000000000000 ) ) ;
#18632=CIRCLE ( 'NONE', #4933, 4.750000000000000000 ) ;
#18645=VERTEX_POINT ( 'NONE', #12781 ) ;
#18658=DIRECTION ( 'NONE',  ( -1.000000000000000000, -0.000000000000000000, -0.000000000000000000 ) ) ;
#18680=VERTEX_POINT ( 'NONE', #13449 ) ;
#18715=ORIENTED_EDGE ( 'NONE', *, *, #7100, .T. ) ;
#18718=CARTESIAN_POINT ( 'NONE',  ( 0.000000000000000000, 3.061616997868383141E-16, -2.500000000000000000 ) ) ;
#18784=AXIS2_PLACEMENT_3D ( 'NONE', #13137, #17736, #10271 ) ;
#18862=CARTESIAN_POINT ( 'NONE',  ( 1.560000000000000053, -1.732050807568877859, -1.752539433813135784E-17 ) ) ;
#18870=DIRECTION ( 'NONE',  ( 0.000000000000000000, 0.000000000000000000, 1.000000000000000000 ) ) ;
ENDSEC;
END-ISO-10303-21;
